ISO-10303-21;
HEADER;
/* Generated by software containing ST-Developer
 * from STEP Tools, Inc. (www.steptools.com) 
 */

FILE_DESCRIPTION(
/* description */ (
'Independent guided parallel-jaw bracket clamp. Two12mm guide rods, re
placeable bronze sleeves, captured swiveling spindle, replaceable jaw 
pads and modeled M16x2 screw. Native slider/revolute joints linked2mm 
per revolution. Nominal opening0..122 with initial28mm. Base and two i
dentical supports welded. Standard fits, weld details and clamp load r
equire engineering selection.'),
/* implementation_level */ '2;1');

FILE_NAME(
/* name */ 'Pivot washer.step',
/* time_stamp */ '2026-11-14T09:15:44-08:00',
/* author */ (''),
/* organization */ (''),
/* preprocessor_version */ 'ST-DEVELOPER v20.2',
/* originating_system */ 'Autodesk Translation Framework v15.17.0.0',
/* authorisation */ '');

FILE_SCHEMA (('AUTOMOTIVE_DESIGN { 1 0 10303 214 3 1 1 }'));
ENDSEC;

DATA;
#10=MECHANICAL_DESIGN_GEOMETRIC_PRESENTATION_REPRESENTATION('',(#925),#105806);
#901=SHAPE_REPRESENTATION_RELATIONSHIP('SRR','None',#105869,#913);
#913=ADVANCED_BREP_SHAPE_REPRESENTATION('',(#937),#105804);
#925=STYLED_ITEM('',(#105930),#937);
#937=MANIFOLD_SOLID_BREP('Body1',#7212);
#994=FACE_BOUND('',#1623,.T.);
#995=FACE_BOUND('',#1625,.T.);
#1053=PLANE('',#7674);
#1054=PLANE('',#7675);
#1293=FACE_OUTER_BOUND('',#1620,.T.);
#1294=FACE_OUTER_BOUND('',#1621,.T.);
#1295=FACE_OUTER_BOUND('',#1622,.T.);
#1296=FACE_OUTER_BOUND('',#1624,.T.);
#1620=EDGE_LOOP('',(#6353,#6354,#6355,#6356));
#1621=EDGE_LOOP('',(#6357,#6358,#6359,#6360));
#1622=EDGE_LOOP('',(#6361));
#1623=EDGE_LOOP('',(#6362));
#1624=EDGE_LOOP('',(#6363));
#1625=EDGE_LOOP('',(#6364));
#1902=LINE('',#88842,#2182);
#1903=LINE('',#88848,#2183);
#2182=VECTOR('',#8623,5.);
#2183=VECTOR('',#8630,10.);
#2315=CIRCLE('',#7669,5.);
#2316=CIRCLE('',#7670,5.);
#2317=CIRCLE('',#7672,10.);
#2318=CIRCLE('',#7673,10.);
#3097=VERTEX_POINT('',#88839);
#3098=VERTEX_POINT('',#88841);
#3099=VERTEX_POINT('',#88845);
#3100=VERTEX_POINT('',#88847);
#4221=EDGE_CURVE('',#3097,#3097,#2315,.T.);
#4222=EDGE_CURVE('',#3097,#3098,#1902,.T.);
#4223=EDGE_CURVE('',#3098,#3098,#2316,.T.);
#4224=EDGE_CURVE('',#3099,#3099,#2317,.T.);
#4225=EDGE_CURVE('',#3099,#3100,#1903,.T.);
#4226=EDGE_CURVE('',#3100,#3100,#2318,.T.);
#6353=ORIENTED_EDGE('',*,*,#4221,.T.);
#6354=ORIENTED_EDGE('',*,*,#4222,.T.);
#6355=ORIENTED_EDGE('',*,*,#4223,.F.);
#6356=ORIENTED_EDGE('',*,*,#4222,.F.);
#6357=ORIENTED_EDGE('',*,*,#4224,.F.);
#6358=ORIENTED_EDGE('',*,*,#4225,.T.);
#6359=ORIENTED_EDGE('',*,*,#4226,.T.);
#6360=ORIENTED_EDGE('',*,*,#4225,.F.);
#6361=ORIENTED_EDGE('',*,*,#4224,.T.);
#6362=ORIENTED_EDGE('',*,*,#4223,.T.);
#6363=ORIENTED_EDGE('',*,*,#4226,.F.);
#6364=ORIENTED_EDGE('',*,*,#4221,.F.);
#6901=CYLINDRICAL_SURFACE('',#7668,5.);
#6902=CYLINDRICAL_SURFACE('',#7671,10.);
#7158=ADVANCED_FACE('',(#1293),#6901,.F.);
#7159=ADVANCED_FACE('',(#1294),#6902,.T.);
#7160=ADVANCED_FACE('',(#1295,#994),#1053,.T.);
#7161=ADVANCED_FACE('',(#1296,#995),#1054,.F.);
#7212=CLOSED_SHELL('',(#7158,#7159,#7160,#7161));
#7667=AXIS2_PLACEMENT_3D('',#88837,#8617,#8618);
#7668=AXIS2_PLACEMENT_3D('',#88838,#8619,#8620);
#7669=AXIS2_PLACEMENT_3D('',#88840,#8621,#8622);
#7670=AXIS2_PLACEMENT_3D('',#88843,#8624,#8625);
#7671=AXIS2_PLACEMENT_3D('',#88844,#8626,#8627);
#7672=AXIS2_PLACEMENT_3D('',#88846,#8628,#8629);
#7673=AXIS2_PLACEMENT_3D('',#88849,#8631,#8632);
#7674=AXIS2_PLACEMENT_3D('',#88850,#8633,#8634);
#7675=AXIS2_PLACEMENT_3D('',#88851,#8635,#8636);
#8617=DIRECTION('axis',(0.,0.,1.));
#8618=DIRECTION('refdir',(1.,0.,0.));
#8619=DIRECTION('center_axis',(0.,0.,1.));
#8620=DIRECTION('ref_axis',(1.,0.,0.));
#8621=DIRECTION('center_axis',(0.,0.,-1.));
#8622=DIRECTION('ref_axis',(1.,0.,0.));
#8623=DIRECTION('',(0.,0.,1.));
#8624=DIRECTION('center_axis',(0.,0.,-1.));
#8625=DIRECTION('ref_axis',(1.,0.,0.));
#8626=DIRECTION('center_axis',(0.,0.,1.));
#8627=DIRECTION('ref_axis',(1.,0.,0.));
#8628=DIRECTION('center_axis',(0.,0.,1.));
#8629=DIRECTION('ref_axis',(1.,0.,0.));
#8630=DIRECTION('',(0.,0.,-1.));
#8631=DIRECTION('center_axis',(0.,0.,1.));
#8632=DIRECTION('ref_axis',(1.,0.,0.));
#8633=DIRECTION('center_axis',(0.,0.,1.));
#8634=DIRECTION('ref_axis',(1.,0.,0.));
#8635=DIRECTION('center_axis',(0.,0.,1.));
#8636=DIRECTION('ref_axis',(1.,0.,0.));
#88837=CARTESIAN_POINT('',(0.,0.,0.));
#88838=CARTESIAN_POINT('Origin',(0.,0.,0.));
#88839=CARTESIAN_POINT('',(-5.,-6.12323399573677E-16,0.));
#88840=CARTESIAN_POINT('Origin',(0.,0.,0.));
#88841=CARTESIAN_POINT('',(-5.,-6.12323399573677E-16,2.));
#88842=CARTESIAN_POINT('',(-5.,-6.12323399573677E-16,0.));
#88843=CARTESIAN_POINT('Origin',(0.,0.,2.));
#88844=CARTESIAN_POINT('Origin',(0.,0.,0.));
#88845=CARTESIAN_POINT('',(-10.,-1.22464679914735E-15,2.));
#88846=CARTESIAN_POINT('Origin',(0.,0.,2.));
#88847=CARTESIAN_POINT('',(-10.,-1.22464679914735E-15,0.));
#88848=CARTESIAN_POINT('',(-10.,-1.22464679914735E-15,0.));
#88849=CARTESIAN_POINT('Origin',(0.,0.,0.));
#88850=CARTESIAN_POINT('Origin',(0.,0.,2.));
#88851=CARTESIAN_POINT('Origin',(0.,0.,0.));
#105790=UNCERTAINTY_MEASURE_WITH_UNIT(LENGTH_MEASURE(0.01),#105807,
'DISTANCE_ACCURACY_VALUE',
'Maximum model space distance between geometric entities at asserted c
onnectivities');
#105792=UNCERTAINTY_MEASURE_WITH_UNIT(LENGTH_MEASURE(0.01),#105807,
'DISTANCE_ACCURACY_VALUE',
'Maximum model space distance between geometric entities at asserted c
onnectivities');
#105804=(
GEOMETRIC_REPRESENTATION_CONTEXT(3)
GLOBAL_UNCERTAINTY_ASSIGNED_CONTEXT((#105790))
GLOBAL_UNIT_ASSIGNED_CONTEXT((#105807,#105809,#105810))
REPRESENTATION_CONTEXT('','3D')
);
#105806=(
GEOMETRIC_REPRESENTATION_CONTEXT(3)
GLOBAL_UNCERTAINTY_ASSIGNED_CONTEXT((#105792))
GLOBAL_UNIT_ASSIGNED_CONTEXT((#105807,#105809,#105810))
REPRESENTATION_CONTEXT('','3D')
);
#105807=(
LENGTH_UNIT()
NAMED_UNIT(*)
SI_UNIT(.MILLI.,.METRE.)
);
#105809=(
NAMED_UNIT(*)
PLANE_ANGLE_UNIT()
SI_UNIT($,.RADIAN.)
);
#105810=(
NAMED_UNIT(*)
SI_UNIT($,.STERADIAN.)
SOLID_ANGLE_UNIT()
);
#105822=SHAPE_DEFINITION_REPRESENTATION(#105835,#105869);
#105835=PRODUCT_DEFINITION_SHAPE('',$,#105883);
#105869=SHAPE_REPRESENTATION('',(#7667),#105804);
#105871=PRODUCT_DEFINITION_CONTEXT('part definition',#105912,'design');
#105883=PRODUCT_DEFINITION('Pivot washer','Pivot washer',#105896,#105871);
#105896=PRODUCT_DEFINITION_FORMATION('',$,#105925);
#105912=APPLICATION_CONTEXT(
'Core Data for Automotive Mechanical Design Process');
#105913=PRODUCT_CONTEXT('part definition',#105912,'mechanical');
#105925=PRODUCT('Pivot washer','Pivot washer',$,(#105913));
#105930=PRESENTATION_STYLE_ASSIGNMENT((#105936));
#105936=SURFACE_STYLE_USAGE(.BOTH.,#105942);
#105942=SURFACE_SIDE_STYLE('',(#105948));
#105948=SURFACE_STYLE_FILL_AREA(#105954);
#105954=FILL_AREA_STYLE('Opaque(185,192,202)',(#105960));
#105960=FILL_AREA_STYLE_COLOUR('Opaque(185,192,202)',#105966);
#105966=COLOUR_RGB('Opaque(185,192,202)',0.725490196078431,0.752941176470588,
0.792156862745098);
ENDSEC;
END-ISO-10303-21;
